ISO-10303-21;
HEADER;
/* Generated by software containing ST-Developer
 * from STEP Tools, Inc. (www.steptools.com) 
 */

FILE_DESCRIPTION(
/* description */ ('PAT-083'),
/* implementation_level */ '2;1');

FILE_NAME(
/* name */ 'Socket Set Screw - M4x6.step',
/* time_stamp */ '2026-10-29T20:18:00-07:00',
/* author */ (''),
/* organization */ (''),
/* preprocessor_version */ 'ST-DEVELOPER v20.2',
/* originating_system */ 'Autodesk Translation Framework v15.17.0.0',
/* authorisation */ '');

FILE_SCHEMA (('AUTOMOTIVE_DESIGN { 1 0 10303 214 3 1 1 }'));
ENDSEC;

DATA;
#10=MECHANICAL_DESIGN_GEOMETRIC_PRESENTATION_REPRESENTATION('',(#252),#8428);
#161=CONICAL_SURFACE('',#4398,0.185,0.785398163397449);
#162=CONICAL_SURFACE('',#4402,0.1625,0.785398163397449);
#204=SHAPE_REPRESENTATION_RELATIONSHIP('SRR','None',#8538,#228);
#228=ADVANCED_BREP_SHAPE_REPRESENTATION('',(#274),#8427);
#252=STYLED_ITEM('',(#8712),#274);
#274=MANIFOLD_SOLID_BREP('Body1',#3700);
#355=FACE_BOUND('',#1037,.T.);
#486=PLANE('',#4389);
#487=PLANE('',#4390);
#488=PLANE('',#4391);
#489=PLANE('',#4392);
#490=PLANE('',#4393);
#491=PLANE('',#4394);
#492=PLANE('',#4395);
#493=PLANE('',#4396);
#494=PLANE('',#4404);
#716=FACE_OUTER_BOUND('',#1029,.T.);
#717=FACE_OUTER_BOUND('',#1030,.T.);
#718=FACE_OUTER_BOUND('',#1031,.T.);
#719=FACE_OUTER_BOUND('',#1032,.T.);
#720=FACE_OUTER_BOUND('',#1033,.T.);
#721=FACE_OUTER_BOUND('',#1034,.T.);
#722=FACE_OUTER_BOUND('',#1035,.T.);
#723=FACE_OUTER_BOUND('',#1036,.T.);
#724=FACE_OUTER_BOUND('',#1038,.T.);
#725=FACE_OUTER_BOUND('',#1039,.T.);
#726=FACE_OUTER_BOUND('',#1040,.T.);
#727=FACE_OUTER_BOUND('',#1041,.T.);
#1029=EDGE_LOOP('',(#3314,#3315,#3316,#3317));
#1030=EDGE_LOOP('',(#3318,#3319,#3320,#3321));
#1031=EDGE_LOOP('',(#3322,#3323,#3324,#3325));
#1032=EDGE_LOOP('',(#3326,#3327,#3328,#3329));
#1033=EDGE_LOOP('',(#3330,#3331,#3332,#3333));
#1034=EDGE_LOOP('',(#3334,#3335,#3336,#3337));
#1035=EDGE_LOOP('',(#3338,#3339,#3340,#3341,#3342,#3343));
#1036=EDGE_LOOP('',(#3344));
#1037=EDGE_LOOP('',(#3345,#3346,#3347,#3348,#3349,#3350));
#1038=EDGE_LOOP('',(#3351,#3352,#3353,#3354));
#1039=EDGE_LOOP('',(#3355,#3356,#3357,#3358));
#1040=EDGE_LOOP('',(#3359,#3360,#3361,#3362));
#1041=EDGE_LOOP('',(#3363));
#1265=LINE('',#8296,#1509);
#1266=LINE('',#8298,#1510);
#1267=LINE('',#8300,#1511);
#1268=LINE('',#8301,#1512);
#1269=LINE('',#8304,#1513);
#1270=LINE('',#8306,#1514);
#1271=LINE('',#8307,#1515);
#1272=LINE('',#8310,#1516);
#1273=LINE('',#8312,#1517);
#1274=LINE('',#8313,#1518);
#1275=LINE('',#8316,#1519);
#1276=LINE('',#8318,#1520);
#1277=LINE('',#8319,#1521);
#1278=LINE('',#8322,#1522);
#1279=LINE('',#8324,#1523);
#1280=LINE('',#8325,#1524);
#1281=LINE('',#8327,#1525);
#1282=LINE('',#8328,#1526);
#1283=LINE('',#8336,#1527);
#1284=LINE('',#8340,#1528);
#1285=LINE('',#8344,#1529);
#1509=VECTOR('',#5507,1.);
#1510=VECTOR('',#5508,1.);
#1511=VECTOR('',#5509,1.);
#1512=VECTOR('',#5510,1.);
#1513=VECTOR('',#5513,1.);
#1514=VECTOR('',#5514,1.);
#1515=VECTOR('',#5515,1.);
#1516=VECTOR('',#5518,1.);
#1517=VECTOR('',#5519,1.);
#1518=VECTOR('',#5520,1.);
#1519=VECTOR('',#5523,1.);
#1520=VECTOR('',#5524,1.);
#1521=VECTOR('',#5525,1.);
#1522=VECTOR('',#5528,1.);
#1523=VECTOR('',#5529,1.);
#1524=VECTOR('',#5530,1.);
#1525=VECTOR('',#5533,1.);
#1526=VECTOR('',#5534,1.);
#1527=VECTOR('',#5545,0.185);
#1528=VECTOR('',#5550,0.2);
#1529=VECTOR('',#5555,0.1625);
#1709=CIRCLE('',#4397,0.17);
#1710=CIRCLE('',#4399,0.1954);
#1711=CIRCLE('',#4401,0.1954);
#1712=CIRCLE('',#4403,0.125);
#1989=VERTEX_POINT('',#8294);
#1990=VERTEX_POINT('',#8295);
#1991=VERTEX_POINT('',#8297);
#1992=VERTEX_POINT('',#8299);
#1993=VERTEX_POINT('',#8303);
#1994=VERTEX_POINT('',#8305);
#1995=VERTEX_POINT('',#8309);
#1996=VERTEX_POINT('',#8311);
#1997=VERTEX_POINT('',#8315);
#1998=VERTEX_POINT('',#8317);
#1999=VERTEX_POINT('',#8321);
#2000=VERTEX_POINT('',#8323);
#2001=VERTEX_POINT('',#8331);
#2002=VERTEX_POINT('',#8334);
#2003=VERTEX_POINT('',#8338);
#2004=VERTEX_POINT('',#8342);
#2433=EDGE_CURVE('',#1989,#1990,#1265,.T.);
#2434=EDGE_CURVE('',#1989,#1991,#1266,.T.);
#2435=EDGE_CURVE('',#1991,#1992,#1267,.T.);
#2436=EDGE_CURVE('',#1990,#1992,#1268,.T.);
#2437=EDGE_CURVE('',#1993,#1989,#1269,.T.);
#2438=EDGE_CURVE('',#1993,#1994,#1270,.T.);
#2439=EDGE_CURVE('',#1994,#1991,#1271,.T.);
#2440=EDGE_CURVE('',#1995,#1993,#1272,.T.);
#2441=EDGE_CURVE('',#1995,#1996,#1273,.T.);
#2442=EDGE_CURVE('',#1996,#1994,#1274,.T.);
#2443=EDGE_CURVE('',#1997,#1995,#1275,.T.);
#2444=EDGE_CURVE('',#1997,#1998,#1276,.T.);
#2445=EDGE_CURVE('',#1998,#1996,#1277,.T.);
#2446=EDGE_CURVE('',#1999,#1997,#1278,.T.);
#2447=EDGE_CURVE('',#1999,#2000,#1279,.T.);
#2448=EDGE_CURVE('',#2000,#1998,#1280,.T.);
#2449=EDGE_CURVE('',#1990,#1999,#1281,.T.);
#2450=EDGE_CURVE('',#1992,#2000,#1282,.T.);
#2451=EDGE_CURVE('',#2001,#2001,#1709,.T.);
#2452=EDGE_CURVE('',#2002,#2002,#1710,.T.);
#2453=EDGE_CURVE('',#2002,#2001,#1283,.T.);
#2454=EDGE_CURVE('',#2003,#2003,#1711,.F.);
#2455=EDGE_CURVE('',#2003,#2002,#1284,.T.);
#2456=EDGE_CURVE('',#2004,#2004,#1712,.T.);
#2457=EDGE_CURVE('',#2004,#2003,#1285,.T.);
#3314=ORIENTED_EDGE('',*,*,#2433,.F.);
#3315=ORIENTED_EDGE('',*,*,#2434,.T.);
#3316=ORIENTED_EDGE('',*,*,#2435,.T.);
#3317=ORIENTED_EDGE('',*,*,#2436,.F.);
#3318=ORIENTED_EDGE('',*,*,#2437,.F.);
#3319=ORIENTED_EDGE('',*,*,#2438,.T.);
#3320=ORIENTED_EDGE('',*,*,#2439,.T.);
#3321=ORIENTED_EDGE('',*,*,#2434,.F.);
#3322=ORIENTED_EDGE('',*,*,#2440,.F.);
#3323=ORIENTED_EDGE('',*,*,#2441,.T.);
#3324=ORIENTED_EDGE('',*,*,#2442,.T.);
#3325=ORIENTED_EDGE('',*,*,#2438,.F.);
#3326=ORIENTED_EDGE('',*,*,#2443,.F.);
#3327=ORIENTED_EDGE('',*,*,#2444,.T.);
#3328=ORIENTED_EDGE('',*,*,#2445,.T.);
#3329=ORIENTED_EDGE('',*,*,#2441,.F.);
#3330=ORIENTED_EDGE('',*,*,#2446,.F.);
#3331=ORIENTED_EDGE('',*,*,#2447,.T.);
#3332=ORIENTED_EDGE('',*,*,#2448,.T.);
#3333=ORIENTED_EDGE('',*,*,#2444,.F.);
#3334=ORIENTED_EDGE('',*,*,#2449,.F.);
#3335=ORIENTED_EDGE('',*,*,#2436,.T.);
#3336=ORIENTED_EDGE('',*,*,#2450,.T.);
#3337=ORIENTED_EDGE('',*,*,#2447,.F.);
#3338=ORIENTED_EDGE('',*,*,#2450,.F.);
#3339=ORIENTED_EDGE('',*,*,#2435,.F.);
#3340=ORIENTED_EDGE('',*,*,#2439,.F.);
#3341=ORIENTED_EDGE('',*,*,#2442,.F.);
#3342=ORIENTED_EDGE('',*,*,#2445,.F.);
#3343=ORIENTED_EDGE('',*,*,#2448,.F.);
#3344=ORIENTED_EDGE('',*,*,#2451,.F.);
#3345=ORIENTED_EDGE('',*,*,#2433,.T.);
#3346=ORIENTED_EDGE('',*,*,#2449,.T.);
#3347=ORIENTED_EDGE('',*,*,#2446,.T.);
#3348=ORIENTED_EDGE('',*,*,#2443,.T.);
#3349=ORIENTED_EDGE('',*,*,#2440,.T.);
#3350=ORIENTED_EDGE('',*,*,#2437,.T.);
#3351=ORIENTED_EDGE('',*,*,#2452,.F.);
#3352=ORIENTED_EDGE('',*,*,#2453,.T.);
#3353=ORIENTED_EDGE('',*,*,#2451,.T.);
#3354=ORIENTED_EDGE('',*,*,#2453,.F.);
#3355=ORIENTED_EDGE('',*,*,#2454,.F.);
#3356=ORIENTED_EDGE('',*,*,#2455,.T.);
#3357=ORIENTED_EDGE('',*,*,#2452,.T.);
#3358=ORIENTED_EDGE('',*,*,#2455,.F.);
#3359=ORIENTED_EDGE('',*,*,#2456,.F.);
#3360=ORIENTED_EDGE('',*,*,#2457,.T.);
#3361=ORIENTED_EDGE('',*,*,#2454,.T.);
#3362=ORIENTED_EDGE('',*,*,#2457,.F.);
#3363=ORIENTED_EDGE('',*,*,#2456,.T.);
#3441=CYLINDRICAL_SURFACE('',#4400,0.1954);
#3663=ADVANCED_FACE('',(#716),#486,.F.);
#3664=ADVANCED_FACE('',(#717),#487,.F.);
#3665=ADVANCED_FACE('',(#718),#488,.F.);
#3666=ADVANCED_FACE('',(#719),#489,.F.);
#3667=ADVANCED_FACE('',(#720),#490,.F.);
#3668=ADVANCED_FACE('',(#721),#491,.F.);
#3669=ADVANCED_FACE('',(#722),#492,.F.);
#3670=ADVANCED_FACE('',(#723,#355),#493,.T.);
#3671=ADVANCED_FACE('',(#724),#161,.T.);
#3672=ADVANCED_FACE('',(#725),#3441,.T.);
#3673=ADVANCED_FACE('',(#726),#162,.T.);
#3674=ADVANCED_FACE('',(#727),#494,.T.);
#3700=CLOSED_SHELL('',(#3663,#3664,#3665,#3666,#3667,#3668,#3669,#3670,
#3671,#3672,#3673,#3674));
#4388=AXIS2_PLACEMENT_3D('',#8292,#5503,#5504);
#4389=AXIS2_PLACEMENT_3D('',#8293,#5505,#5506);
#4390=AXIS2_PLACEMENT_3D('',#8302,#5511,#5512);
#4391=AXIS2_PLACEMENT_3D('',#8308,#5516,#5517);
#4392=AXIS2_PLACEMENT_3D('',#8314,#5521,#5522);
#4393=AXIS2_PLACEMENT_3D('',#8320,#5526,#5527);
#4394=AXIS2_PLACEMENT_3D('',#8326,#5531,#5532);
#4395=AXIS2_PLACEMENT_3D('',#8329,#5535,#5536);
#4396=AXIS2_PLACEMENT_3D('',#8330,#5537,#5538);
#4397=AXIS2_PLACEMENT_3D('',#8332,#5539,#5540);
#4398=AXIS2_PLACEMENT_3D('',#8333,#5541,#5542);
#4399=AXIS2_PLACEMENT_3D('',#8335,#5543,#5544);
#4400=AXIS2_PLACEMENT_3D('',#8337,#5546,#5547);
#4401=AXIS2_PLACEMENT_3D('',#8339,#5548,#5549);
#4402=AXIS2_PLACEMENT_3D('',#8341,#5551,#5552);
#4403=AXIS2_PLACEMENT_3D('',#8343,#5553,#5554);
#4404=AXIS2_PLACEMENT_3D('',#8345,#5556,#5557);
#5503=DIRECTION('axis',(0.,0.,1.));
#5504=DIRECTION('refdir',(1.,0.,0.));
#5505=DIRECTION('center_axis',(0.866025403784439,0.,-0.5));
#5506=DIRECTION('ref_axis',(0.5,0.,0.866025403784439));
#5507=DIRECTION('',(0.5,0.,0.866025403784439));
#5508=DIRECTION('',(0.,-1.,0.));
#5509=DIRECTION('',(0.5,0.,0.866025403784439));
#5510=DIRECTION('',(0.,-1.,0.));
#5511=DIRECTION('center_axis',(1.20185167898973E-16,0.,-1.));
#5512=DIRECTION('ref_axis',(1.,0.,1.20185167898973E-16));
#5513=DIRECTION('',(1.,0.,1.20185167898973E-16));
#5514=DIRECTION('',(0.,-1.,0.));
#5515=DIRECTION('',(1.,0.,1.20185167898973E-16));
#5516=DIRECTION('center_axis',(-0.866025403784439,0.,-0.5));
#5517=DIRECTION('ref_axis',(0.5,0.,-0.866025403784439));
#5518=DIRECTION('',(0.5,0.,-0.866025403784439));
#5519=DIRECTION('',(0.,-1.,0.));
#5520=DIRECTION('',(0.5,0.,-0.866025403784439));
#5521=DIRECTION('center_axis',(-0.866025403784439,0.,0.5));
#5522=DIRECTION('ref_axis',(-0.5,0.,-0.866025403784439));
#5523=DIRECTION('',(-0.5,0.,-0.866025403784439));
#5524=DIRECTION('',(0.,-1.,0.));
#5525=DIRECTION('',(-0.5,0.,-0.866025403784439));
#5526=DIRECTION('center_axis',(-2.40370335797945E-16,0.,1.));
#5527=DIRECTION('ref_axis',(-1.,0.,-2.40370335797945E-16));
#5528=DIRECTION('',(-1.,0.,-2.40370335797945E-16));
#5529=DIRECTION('',(0.,-1.,0.));
#5530=DIRECTION('',(-1.,0.,-2.40370335797945E-16));
#5531=DIRECTION('center_axis',(0.866025403784439,0.,0.5));
#5532=DIRECTION('ref_axis',(-0.5,0.,0.866025403784439));
#5533=DIRECTION('',(-0.5,0.,0.866025403784439));
#5534=DIRECTION('',(-0.5,0.,0.866025403784439));
#5535=DIRECTION('center_axis',(0.,-1.,0.));
#5536=DIRECTION('ref_axis',(0.,0.,-1.));
#5537=DIRECTION('center_axis',(0.,1.,0.));
#5538=DIRECTION('ref_axis',(0.,0.,1.));
#5539=DIRECTION('center_axis',(0.,-1.,0.));
#5540=DIRECTION('ref_axis',(1.,0.,0.));
#5541=DIRECTION('center_axis',(0.,-1.,0.));
#5542=DIRECTION('ref_axis',(1.,0.,0.));
#5543=DIRECTION('center_axis',(0.,-1.,0.));
#5544=DIRECTION('ref_axis',(1.,0.,0.));
#5545=DIRECTION('',(0.707106781186548,0.707106781186547,8.65956056235494E-17));
#5546=DIRECTION('center_axis',(0.,-1.,0.));
#5547=DIRECTION('ref_axis',(1.,0.,0.));
#5548=DIRECTION('center_axis',(0.,1.,0.));
#5549=DIRECTION('ref_axis',(1.,0.,0.));
#5550=DIRECTION('',(0.,1.,0.));
#5551=DIRECTION('center_axis',(0.,1.,0.));
#5552=DIRECTION('ref_axis',(1.,0.,0.));
#5553=DIRECTION('center_axis',(0.,-1.,0.));
#5554=DIRECTION('ref_axis',(1.,0.,0.));
#5555=DIRECTION('',(-0.707106781186548,0.707106781186547,-8.65956056235494E-17));
#5556=DIRECTION('center_axis',(0.,-1.,0.));
#5557=DIRECTION('ref_axis',(0.,0.,-1.));
#8292=CARTESIAN_POINT('',(0.,0.,0.));
#8293=CARTESIAN_POINT('Origin',(0.0577350269189626,0.,-0.1));
#8294=CARTESIAN_POINT('',(0.0577350269189626,0.,-0.1));
#8295=CARTESIAN_POINT('',(0.115470053837925,0.,0.));
#8296=CARTESIAN_POINT('',(0.0934187836487032,0.,-0.0381939203391614));
#8297=CARTESIAN_POINT('',(0.0577350269189626,-0.2,-0.1));
#8298=CARTESIAN_POINT('',(0.0577350269189626,0.,-0.1));
#8299=CARTESIAN_POINT('',(0.115470053837925,-0.2,0.));
#8300=CARTESIAN_POINT('',(0.115470053837925,-0.2,0.));
#8301=CARTESIAN_POINT('',(0.115470053837925,0.,0.));
#8302=CARTESIAN_POINT('Origin',(-0.0577350269189626,0.,-0.1));
#8303=CARTESIAN_POINT('',(-0.0577350269189626,0.,-0.1));
#8304=CARTESIAN_POINT('',(0.0561324865405187,0.,-0.1));
#8305=CARTESIAN_POINT('',(-0.0577350269189626,-0.2,-0.1));
#8306=CARTESIAN_POINT('',(-0.0577350269189626,0.,-0.1));
#8307=CARTESIAN_POINT('',(0.0577350269189626,-0.2,-0.1));
#8308=CARTESIAN_POINT('Origin',(-0.115470053837925,0.,-1.38777878078145E-17));
#8309=CARTESIAN_POINT('',(-0.115470053837925,0.,-1.41410031829988E-17));
#8310=CARTESIAN_POINT('',(-0.0797862971081845,0.,-0.0618060796608387));
#8311=CARTESIAN_POINT('',(-0.115470053837925,-0.2,-1.38777878078145E-17));
#8312=CARTESIAN_POINT('',(-0.115470053837925,0.,-1.41410031829988E-17));
#8313=CARTESIAN_POINT('',(-0.0577350269189626,-0.2,-0.1));
#8314=CARTESIAN_POINT('Origin',(-0.0577350269189626,0.,0.1));
#8315=CARTESIAN_POINT('',(-0.0577350269189626,0.,0.1));
#8316=CARTESIAN_POINT('',(-0.0509187836487033,0.,0.111806079660839));
#8317=CARTESIAN_POINT('',(-0.0577350269189626,-0.2,0.1));
#8318=CARTESIAN_POINT('',(-0.0577350269189626,0.,0.1));
#8319=CARTESIAN_POINT('',(-0.115470053837925,-0.2,-1.41410031829988E-17));
#8320=CARTESIAN_POINT('Origin',(0.0577350269189626,0.,0.1));
#8321=CARTESIAN_POINT('',(0.0577350269189626,0.,0.1));
#8322=CARTESIAN_POINT('',(0.113867513459481,0.,0.1));
#8323=CARTESIAN_POINT('',(0.0577350269189626,-0.2,0.1));
#8324=CARTESIAN_POINT('',(0.0577350269189626,0.,0.1));
#8325=CARTESIAN_POINT('',(-0.0577350269189626,-0.2,0.1));
#8326=CARTESIAN_POINT('Origin',(0.115470053837925,0.,0.));
#8327=CARTESIAN_POINT('',(0.122286297108185,0.,-0.0118060796608386));
#8328=CARTESIAN_POINT('',(0.0577350269189626,-0.2,0.1));
#8329=CARTESIAN_POINT('Origin',(0.,-0.2,0.));
#8330=CARTESIAN_POINT('Origin',(0.17,0.,0.));
#8331=CARTESIAN_POINT('',(-0.17,-8.67361737988404E-18,-2.0818995585505E-17));
#8332=CARTESIAN_POINT('Origin',(0.,0.,0.));
#8333=CARTESIAN_POINT('Origin',(0.,-0.015,0.));
#8334=CARTESIAN_POINT('',(-0.1954,-0.0254,-2.39295984553393E-17));
#8335=CARTESIAN_POINT('Origin',(0.,-0.0254,0.));
#8336=CARTESIAN_POINT('',(-0.185,-0.015,-2.2655965784226E-17));
#8337=CARTESIAN_POINT('Origin',(0.,-0.2775,0.));
#8338=CARTESIAN_POINT('',(-0.1954,-0.5296,2.39295984553393E-17));
#8339=CARTESIAN_POINT('Origin',(0.,-0.5296,0.));
#8340=CARTESIAN_POINT('',(-0.1954,-0.2775,-2.39295984553393E-17));
#8341=CARTESIAN_POINT('Origin',(0.,-0.5625,0.));
#8342=CARTESIAN_POINT('',(-0.125,-0.6,-1.53080849893419E-17));
#8343=CARTESIAN_POINT('Origin',(0.,-0.6,0.));
#8344=CARTESIAN_POINT('',(-0.1625,-0.5625,-1.99005104861445E-17));
#8345=CARTESIAN_POINT('Origin',(0.,-0.6,0.));
#8401=UNCERTAINTY_MEASURE_WITH_UNIT(LENGTH_MEASURE(0.001),#8429,
'DISTANCE_ACCURACY_VALUE',
'Maximum model space distance between geometric entities at asserted c
onnectivities');
#8402=UNCERTAINTY_MEASURE_WITH_UNIT(LENGTH_MEASURE(0.001),#8429,
'DISTANCE_ACCURACY_VALUE',
'Maximum model space distance between geometric entities at asserted c
onnectivities');
#8427=(
GEOMETRIC_REPRESENTATION_CONTEXT(3)
GLOBAL_UNCERTAINTY_ASSIGNED_CONTEXT((#8401))
GLOBAL_UNIT_ASSIGNED_CONTEXT((#8429,#8431,#8432))
REPRESENTATION_CONTEXT('','3D')
);
#8428=(
GEOMETRIC_REPRESENTATION_CONTEXT(3)
GLOBAL_UNCERTAINTY_ASSIGNED_CONTEXT((#8402))
GLOBAL_UNIT_ASSIGNED_CONTEXT((#8429,#8431,#8432))
REPRESENTATION_CONTEXT('','3D')
);
#8429=(
LENGTH_UNIT()
NAMED_UNIT(*)
SI_UNIT(.CENTI.,.METRE.)
);
#8431=(
NAMED_UNIT(*)
PLANE_ANGLE_UNIT()
SI_UNIT($,.RADIAN.)
);
#8432=(
NAMED_UNIT(*)
SI_UNIT($,.STERADIAN.)
SOLID_ANGLE_UNIT()
);
#8457=SHAPE_DEFINITION_REPRESENTATION(#8482,#8538);
#8482=PRODUCT_DEFINITION_SHAPE('',$,#8564);
#8538=SHAPE_REPRESENTATION('',(#4388),#8427);
#8539=PRODUCT_DEFINITION_CONTEXT('part definition',#8616,'design');
#8564=PRODUCT_DEFINITION('Socket Set Screw - M4x6',
'Socket Set Screw - M4x6',#8589,#8539);
#8589=PRODUCT_DEFINITION_FORMATION('',$,#8642);
#8616=APPLICATION_CONTEXT(
'Core Data for Automotive Mechanical Design Process');
#8617=PRODUCT_CONTEXT('part definition',#8616,'mechanical');
#8642=PRODUCT('Socket Set Screw - M4x6','Socket Set Screw - M4x6',
'Socket Set Screw - M4x6',(#8617));
#8706=COLOUR_RGB('Black',0.12,0.14,0.17);
#8707=FILL_AREA_STYLE_COLOUR('',#8706);
#8708=FILL_AREA_STYLE('',(#8707));
#8709=SURFACE_STYLE_FILL_AREA(#8708);
#8710=SURFACE_SIDE_STYLE('',(#8709));
#8711=SURFACE_STYLE_USAGE(.BOTH.,#8710);
#8712=PRESENTATION_STYLE_ASSIGNMENT((#8711));
ENDSEC;
END-ISO-10303-21;
